ISO-10303-21;
HEADER;
/* Generated by software containing ST-Developer
 * from STEP Tools, Inc. (www.steptools.com) 
 */

FILE_DESCRIPTION(
/* description */ (''),
/* implementation_level */ '2;1');

FILE_NAME(
/* name */ 'Front_Block.step',
/* time_stamp */ '2026-10-19T02:00:06+06:00',
/* author */ (''),
/* organization */ (''),
/* preprocessor_version */ 'ST-DEVELOPER v20.2',
/* originating_system */ 'Autodesk Translation Framework v15.15.0.0',
/* authorisation */ '');

FILE_SCHEMA (('AUTOMOTIVE_DESIGN { 1 0 10303 214 3 1 1 }'));
ENDSEC;

DATA;
#10=MECHANICAL_DESIGN_GEOMETRIC_PRESENTATION_REPRESENTATION('',(#108),#4833);
#67=ELLIPSE('',#2891,1.08239220029239,1.);
#68=ELLIPSE('',#2892,1.08239220029239,1.);
#69=ELLIPSE('',#2894,1.08239220029239,1.);
#70=ELLIPSE('',#2896,1.08239220029239,1.);
#71=ELLIPSE('',#2898,1.08239220029239,1.);
#72=ELLIPSE('',#2899,1.08239220029239,1.);
#73=ELLIPSE('',#2901,1.0823922002924,1.);
#74=ELLIPSE('',#2904,1.08239220029239,1.);
#86=SHAPE_REPRESENTATION_RELATIONSHIP('SRR','None',#4877,#97);
#97=ADVANCED_BREP_SHAPE_REPRESENTATION('',(#119),#4825);
#108=STYLED_ITEM('',(#4971),#119);
#119=MANIFOLD_SOLID_BREP('Front_Block',#2690);
#190=PLANE('',#2906);
#191=PLANE('',#2907);
#192=PLANE('',#2908);
#193=PLANE('',#2909);
#194=PLANE('',#2910);
#195=PLANE('',#2911);
#196=PLANE('',#2912);
#197=PLANE('',#2913);
#198=PLANE('',#2914);
#199=PLANE('',#2915);
#307=FACE_OUTER_BOUND('',#480,.T.);
#308=FACE_OUTER_BOUND('',#481,.T.);
#309=FACE_OUTER_BOUND('',#482,.T.);
#310=FACE_OUTER_BOUND('',#483,.T.);
#311=FACE_OUTER_BOUND('',#484,.T.);
#312=FACE_OUTER_BOUND('',#485,.T.);
#313=FACE_OUTER_BOUND('',#486,.T.);
#314=FACE_OUTER_BOUND('',#487,.T.);
#315=FACE_OUTER_BOUND('',#488,.T.);
#316=FACE_OUTER_BOUND('',#489,.T.);
#317=FACE_OUTER_BOUND('',#490,.T.);
#318=FACE_OUTER_BOUND('',#491,.T.);
#319=FACE_OUTER_BOUND('',#492,.T.);
#320=FACE_OUTER_BOUND('',#493,.T.);
#321=FACE_OUTER_BOUND('',#494,.T.);
#322=FACE_OUTER_BOUND('',#495,.T.);
#323=FACE_OUTER_BOUND('',#496,.T.);
#324=FACE_OUTER_BOUND('',#497,.T.);
#480=EDGE_LOOP('',(#1903,#1904,#1905,#1906));
#481=EDGE_LOOP('',(#1907,#1908,#1909,#1910));
#482=EDGE_LOOP('',(#1911,#1912,#1913,#1914));
#483=EDGE_LOOP('',(#1915,#1916,#1917,#1918));
#484=EDGE_LOOP('',(#1919,#1920,#1921,#1922));
#485=EDGE_LOOP('',(#1923,#1924,#1925,#1926));
#486=EDGE_LOOP('',(#1927,#1928,#1929,#1930));
#487=EDGE_LOOP('',(#1931,#1932,#1933,#1934));
#488=EDGE_LOOP('',(#1935,#1936,#1937,#1938));
#489=EDGE_LOOP('',(#1939,#1940,#1941,#1942));
#490=EDGE_LOOP('',(#1943,#1944,#1945,#1946));
#491=EDGE_LOOP('',(#1947,#1948,#1949,#1950));
#492=EDGE_LOOP('',(#1951,#1952,#1953,#1954,#1955,#1956,#1957,#1958));
#493=EDGE_LOOP('',(#1959,#1960,#1961,#1962));
#494=EDGE_LOOP('',(#1963,#1964,#1965,#1966));
#495=EDGE_LOOP('',(#1967,#1968,#1969,#1970));
#496=EDGE_LOOP('',(#1971,#1972,#1973,#1974));
#497=EDGE_LOOP('',(#1975,#1976,#1977,#1978,#1979,#1980,#1981,#1982));
#664=LINE('',#4036,#918);
#665=LINE('',#4040,#919);
#666=LINE('',#4044,#920);
#667=LINE('',#4047,#921);
#668=LINE('',#4050,#922);
#669=LINE('',#4053,#923);
#670=LINE('',#4057,#924);
#671=LINE('',#4061,#925);
#672=LINE('',#4065,#926);
#673=LINE('',#4067,#927);
#674=LINE('',#4070,#928);
#675=LINE('',#4071,#929);
#676=LINE('',#4074,#930);
#677=LINE('',#4076,#931);
#678=LINE('',#4079,#932);
#679=LINE('',#4080,#933);
#680=LINE('',#4083,#934);
#681=LINE('',#4085,#935);
#682=LINE('',#4086,#936);
#683=LINE('',#4089,#937);
#684=LINE('',#4090,#938);
#685=LINE('',#4093,#939);
#686=LINE('',#4094,#940);
#687=LINE('',#4097,#941);
#688=LINE('',#4098,#942);
#689=LINE('',#4102,#943);
#690=LINE('',#4104,#944);
#691=LINE('',#4105,#945);
#692=LINE('',#4107,#946);
#693=LINE('',#4110,#947);
#694=LINE('',#4111,#948);
#695=LINE('',#4113,#949);
#918=VECTOR('',#3269,10.);
#919=VECTOR('',#3272,10.);
#920=VECTOR('',#3277,10.);
#921=VECTOR('',#3280,10.);
#922=VECTOR('',#3283,10.);
#923=VECTOR('',#3286,10.);
#924=VECTOR('',#3289,10.);
#925=VECTOR('',#3292,10.);
#926=VECTOR('',#3297,10.);
#927=VECTOR('',#3298,10.);
#928=VECTOR('',#3303,10.);
#929=VECTOR('',#3304,10.);
#930=VECTOR('',#3307,10.);
#931=VECTOR('',#3308,10.);
#932=VECTOR('',#3313,10.);
#933=VECTOR('',#3314,10.);
#934=VECTOR('',#3317,10.);
#935=VECTOR('',#3318,10.);
#936=VECTOR('',#3319,10.);
#937=VECTOR('',#3322,10.);
#938=VECTOR('',#3323,10.);
#939=VECTOR('',#3326,10.);
#940=VECTOR('',#3327,10.);
#941=VECTOR('',#3330,10.);
#942=VECTOR('',#3331,10.);
#943=VECTOR('',#3336,10.);
#944=VECTOR('',#3337,10.);
#945=VECTOR('',#3338,10.);
#946=VECTOR('',#3341,10.);
#947=VECTOR('',#3344,10.);
#948=VECTOR('',#3345,10.);
#949=VECTOR('',#3348,10.);
#1247=VERTEX_POINT('',#4034);
#1248=VERTEX_POINT('',#4035);
#1249=VERTEX_POINT('',#4037);
#1250=VERTEX_POINT('',#4039);
#1251=VERTEX_POINT('',#4043);
#1252=VERTEX_POINT('',#4045);
#1253=VERTEX_POINT('',#4049);
#1254=VERTEX_POINT('',#4051);
#1255=VERTEX_POINT('',#4055);
#1256=VERTEX_POINT('',#4056);
#1257=VERTEX_POINT('',#4058);
#1258=VERTEX_POINT('',#4060);
#1259=VERTEX_POINT('',#4064);
#1260=VERTEX_POINT('',#4066);
#1261=VERTEX_POINT('',#4073);
#1262=VERTEX_POINT('',#4075);
#1263=VERTEX_POINT('',#4082);
#1264=VERTEX_POINT('',#4084);
#1265=VERTEX_POINT('',#4088);
#1266=VERTEX_POINT('',#4092);
#1267=VERTEX_POINT('',#4096);
#1268=VERTEX_POINT('',#4101);
#1269=VERTEX_POINT('',#4103);
#1270=VERTEX_POINT('',#4109);
#1492=EDGE_CURVE('',#1247,#1248,#664,.T.);
#1493=EDGE_CURVE('',#1248,#1249,#67,.T.);
#1494=EDGE_CURVE('',#1249,#1250,#665,.T.);
#1495=EDGE_CURVE('',#1250,#1247,#68,.T.);
#1496=EDGE_CURVE('',#1248,#1251,#666,.T.);
#1497=EDGE_CURVE('',#1251,#1252,#69,.T.);
#1498=EDGE_CURVE('',#1252,#1249,#667,.T.);
#1499=EDGE_CURVE('',#1251,#1253,#668,.T.);
#1500=EDGE_CURVE('',#1253,#1254,#70,.T.);
#1501=EDGE_CURVE('',#1254,#1252,#669,.T.);
#1502=EDGE_CURVE('',#1255,#1256,#670,.T.);
#1503=EDGE_CURVE('',#1256,#1257,#71,.T.);
#1504=EDGE_CURVE('',#1257,#1258,#671,.T.);
#1505=EDGE_CURVE('',#1258,#1255,#72,.T.);
#1506=EDGE_CURVE('',#1259,#1257,#672,.T.);
#1507=EDGE_CURVE('',#1256,#1260,#673,.T.);
#1508=EDGE_CURVE('',#1260,#1259,#73,.T.);
#1509=EDGE_CURVE('',#1253,#1255,#674,.T.);
#1510=EDGE_CURVE('',#1258,#1254,#675,.T.);
#1511=EDGE_CURVE('',#1261,#1259,#676,.T.);
#1512=EDGE_CURVE('',#1260,#1262,#677,.T.);
#1513=EDGE_CURVE('',#1262,#1261,#74,.T.);
#1514=EDGE_CURVE('',#1250,#1261,#678,.T.);
#1515=EDGE_CURVE('',#1262,#1247,#679,.T.);
#1516=EDGE_CURVE('',#1252,#1263,#680,.T.);
#1517=EDGE_CURVE('',#1264,#1263,#681,.T.);
#1518=EDGE_CURVE('',#1264,#1249,#682,.T.);
#1519=EDGE_CURVE('',#1265,#1254,#683,.T.);
#1520=EDGE_CURVE('',#1263,#1265,#684,.T.);
#1521=EDGE_CURVE('',#1258,#1266,#685,.T.);
#1522=EDGE_CURVE('',#1265,#1266,#686,.T.);
#1523=EDGE_CURVE('',#1267,#1257,#687,.T.);
#1524=EDGE_CURVE('',#1266,#1267,#688,.T.);
#1525=EDGE_CURVE('',#1268,#1261,#689,.T.);
#1526=EDGE_CURVE('',#1269,#1268,#690,.T.);
#1527=EDGE_CURVE('',#1259,#1269,#691,.T.);
#1528=EDGE_CURVE('',#1267,#1269,#692,.T.);
#1529=EDGE_CURVE('',#1270,#1264,#693,.T.);
#1530=EDGE_CURVE('',#1250,#1270,#694,.T.);
#1531=EDGE_CURVE('',#1268,#1270,#695,.T.);
#1903=ORIENTED_EDGE('',*,*,#1492,.T.);
#1904=ORIENTED_EDGE('',*,*,#1493,.T.);
#1905=ORIENTED_EDGE('',*,*,#1494,.T.);
#1906=ORIENTED_EDGE('',*,*,#1495,.T.);
#1907=ORIENTED_EDGE('',*,*,#1496,.T.);
#1908=ORIENTED_EDGE('',*,*,#1497,.T.);
#1909=ORIENTED_EDGE('',*,*,#1498,.T.);
#1910=ORIENTED_EDGE('',*,*,#1493,.F.);
#1911=ORIENTED_EDGE('',*,*,#1499,.T.);
#1912=ORIENTED_EDGE('',*,*,#1500,.T.);
#1913=ORIENTED_EDGE('',*,*,#1501,.T.);
#1914=ORIENTED_EDGE('',*,*,#1497,.F.);
#1915=ORIENTED_EDGE('',*,*,#1502,.T.);
#1916=ORIENTED_EDGE('',*,*,#1503,.T.);
#1917=ORIENTED_EDGE('',*,*,#1504,.T.);
#1918=ORIENTED_EDGE('',*,*,#1505,.T.);
#1919=ORIENTED_EDGE('',*,*,#1506,.T.);
#1920=ORIENTED_EDGE('',*,*,#1503,.F.);
#1921=ORIENTED_EDGE('',*,*,#1507,.T.);
#1922=ORIENTED_EDGE('',*,*,#1508,.T.);
#1923=ORIENTED_EDGE('',*,*,#1509,.T.);
#1924=ORIENTED_EDGE('',*,*,#1505,.F.);
#1925=ORIENTED_EDGE('',*,*,#1510,.T.);
#1926=ORIENTED_EDGE('',*,*,#1500,.F.);
#1927=ORIENTED_EDGE('',*,*,#1511,.T.);
#1928=ORIENTED_EDGE('',*,*,#1508,.F.);
#1929=ORIENTED_EDGE('',*,*,#1512,.T.);
#1930=ORIENTED_EDGE('',*,*,#1513,.T.);
#1931=ORIENTED_EDGE('',*,*,#1514,.T.);
#1932=ORIENTED_EDGE('',*,*,#1513,.F.);
#1933=ORIENTED_EDGE('',*,*,#1515,.T.);
#1934=ORIENTED_EDGE('',*,*,#1495,.F.);
#1935=ORIENTED_EDGE('',*,*,#1498,.F.);
#1936=ORIENTED_EDGE('',*,*,#1516,.T.);
#1937=ORIENTED_EDGE('',*,*,#1517,.F.);
#1938=ORIENTED_EDGE('',*,*,#1518,.T.);
#1939=ORIENTED_EDGE('',*,*,#1501,.F.);
#1940=ORIENTED_EDGE('',*,*,#1519,.F.);
#1941=ORIENTED_EDGE('',*,*,#1520,.F.);
#1942=ORIENTED_EDGE('',*,*,#1516,.F.);
#1943=ORIENTED_EDGE('',*,*,#1510,.F.);
#1944=ORIENTED_EDGE('',*,*,#1521,.T.);
#1945=ORIENTED_EDGE('',*,*,#1522,.F.);
#1946=ORIENTED_EDGE('',*,*,#1519,.T.);
#1947=ORIENTED_EDGE('',*,*,#1504,.F.);
#1948=ORIENTED_EDGE('',*,*,#1523,.F.);
#1949=ORIENTED_EDGE('',*,*,#1524,.F.);
#1950=ORIENTED_EDGE('',*,*,#1521,.F.);
#1951=ORIENTED_EDGE('',*,*,#1502,.F.);
#1952=ORIENTED_EDGE('',*,*,#1509,.F.);
#1953=ORIENTED_EDGE('',*,*,#1499,.F.);
#1954=ORIENTED_EDGE('',*,*,#1496,.F.);
#1955=ORIENTED_EDGE('',*,*,#1492,.F.);
#1956=ORIENTED_EDGE('',*,*,#1515,.F.);
#1957=ORIENTED_EDGE('',*,*,#1512,.F.);
#1958=ORIENTED_EDGE('',*,*,#1507,.F.);
#1959=ORIENTED_EDGE('',*,*,#1511,.F.);
#1960=ORIENTED_EDGE('',*,*,#1525,.F.);
#1961=ORIENTED_EDGE('',*,*,#1526,.F.);
#1962=ORIENTED_EDGE('',*,*,#1527,.F.);
#1963=ORIENTED_EDGE('',*,*,#1506,.F.);
#1964=ORIENTED_EDGE('',*,*,#1527,.T.);
#1965=ORIENTED_EDGE('',*,*,#1528,.F.);
#1966=ORIENTED_EDGE('',*,*,#1523,.T.);
#1967=ORIENTED_EDGE('',*,*,#1494,.F.);
#1968=ORIENTED_EDGE('',*,*,#1518,.F.);
#1969=ORIENTED_EDGE('',*,*,#1529,.F.);
#1970=ORIENTED_EDGE('',*,*,#1530,.F.);
#1971=ORIENTED_EDGE('',*,*,#1514,.F.);
#1972=ORIENTED_EDGE('',*,*,#1530,.T.);
#1973=ORIENTED_EDGE('',*,*,#1531,.F.);
#1974=ORIENTED_EDGE('',*,*,#1525,.T.);
#1975=ORIENTED_EDGE('',*,*,#1524,.T.);
#1976=ORIENTED_EDGE('',*,*,#1528,.T.);
#1977=ORIENTED_EDGE('',*,*,#1526,.T.);
#1978=ORIENTED_EDGE('',*,*,#1531,.T.);
#1979=ORIENTED_EDGE('',*,*,#1529,.T.);
#1980=ORIENTED_EDGE('',*,*,#1517,.T.);
#1981=ORIENTED_EDGE('',*,*,#1520,.T.);
#1982=ORIENTED_EDGE('',*,*,#1522,.T.);
#2486=CYLINDRICAL_SURFACE('',#2890,1.);
#2487=CYLINDRICAL_SURFACE('',#2893,1.);
#2488=CYLINDRICAL_SURFACE('',#2895,1.);
#2489=CYLINDRICAL_SURFACE('',#2897,1.);
#2490=CYLINDRICAL_SURFACE('',#2900,1.);
#2491=CYLINDRICAL_SURFACE('',#2902,1.);
#2492=CYLINDRICAL_SURFACE('',#2903,1.);
#2493=CYLINDRICAL_SURFACE('',#2905,1.);
#2565=ADVANCED_FACE('',(#307),#2486,.T.);
#2566=ADVANCED_FACE('',(#308),#2487,.T.);
#2567=ADVANCED_FACE('',(#309),#2488,.T.);
#2568=ADVANCED_FACE('',(#310),#2489,.T.);
#2569=ADVANCED_FACE('',(#311),#2490,.T.);
#2570=ADVANCED_FACE('',(#312),#2491,.T.);
#2571=ADVANCED_FACE('',(#313),#2492,.T.);
#2572=ADVANCED_FACE('',(#314),#2493,.T.);
#2573=ADVANCED_FACE('',(#315),#190,.F.);
#2574=ADVANCED_FACE('',(#316),#191,.F.);
#2575=ADVANCED_FACE('',(#317),#192,.F.);
#2576=ADVANCED_FACE('',(#318),#193,.F.);
#2577=ADVANCED_FACE('',(#319),#194,.F.);
#2578=ADVANCED_FACE('',(#320),#195,.F.);
#2579=ADVANCED_FACE('',(#321),#196,.F.);
#2580=ADVANCED_FACE('',(#322),#197,.F.);
#2581=ADVANCED_FACE('',(#323),#198,.F.);
#2582=ADVANCED_FACE('',(#324),#199,.T.);
#2690=CLOSED_SHELL('',(#2565,#2566,#2567,#2568,#2569,#2570,#2571,#2572,
#2573,#2574,#2575,#2576,#2577,#2578,#2579,#2580,#2581,#2582));
#2889=AXIS2_PLACEMENT_3D('',#4032,#3265,#3266);
#2890=AXIS2_PLACEMENT_3D('',#4033,#3267,#3268);
#2891=AXIS2_PLACEMENT_3D('',#4038,#3270,#3271);
#2892=AXIS2_PLACEMENT_3D('',#4041,#3273,#3274);
#2893=AXIS2_PLACEMENT_3D('',#4042,#3275,#3276);
#2894=AXIS2_PLACEMENT_3D('',#4046,#3278,#3279);
#2895=AXIS2_PLACEMENT_3D('',#4048,#3281,#3282);
#2896=AXIS2_PLACEMENT_3D('',#4052,#3284,#3285);
#2897=AXIS2_PLACEMENT_3D('',#4054,#3287,#3288);
#2898=AXIS2_PLACEMENT_3D('',#4059,#3290,#3291);
#2899=AXIS2_PLACEMENT_3D('',#4062,#3293,#3294);
#2900=AXIS2_PLACEMENT_3D('',#4063,#3295,#3296);
#2901=AXIS2_PLACEMENT_3D('',#4068,#3299,#3300);
#2902=AXIS2_PLACEMENT_3D('',#4069,#3301,#3302);
#2903=AXIS2_PLACEMENT_3D('',#4072,#3305,#3306);
#2904=AXIS2_PLACEMENT_3D('',#4077,#3309,#3310);
#2905=AXIS2_PLACEMENT_3D('',#4078,#3311,#3312);
#2906=AXIS2_PLACEMENT_3D('',#4081,#3315,#3316);
#2907=AXIS2_PLACEMENT_3D('',#4087,#3320,#3321);
#2908=AXIS2_PLACEMENT_3D('',#4091,#3324,#3325);
#2909=AXIS2_PLACEMENT_3D('',#4095,#3328,#3329);
#2910=AXIS2_PLACEMENT_3D('',#4099,#3332,#3333);
#2911=AXIS2_PLACEMENT_3D('',#4100,#3334,#3335);
#2912=AXIS2_PLACEMENT_3D('',#4106,#3339,#3340);
#2913=AXIS2_PLACEMENT_3D('',#4108,#3342,#3343);
#2914=AXIS2_PLACEMENT_3D('',#4112,#3346,#3347);
#2915=AXIS2_PLACEMENT_3D('',#4114,#3349,#3350);
#3265=DIRECTION('axis',(0.,0.,1.));
#3266=DIRECTION('refdir',(1.,0.,0.));
#3267=DIRECTION('center_axis',(0.,0.707106781186548,0.707106781186548));
#3268=DIRECTION('ref_axis',(-0.707106781186553,-0.499999999999996,0.499999999999996));
#3269=DIRECTION('',(0.,-0.707106781186548,-0.707106781186548));
#3270=DIRECTION('center_axis',(0.,0.382683432365092,0.923879532511286));
#3271=DIRECTION('ref_axis',(0.,-0.923879532511286,0.382683432365091));
#3272=DIRECTION('',(0.,0.707106781186548,0.707106781186548));
#3273=DIRECTION('center_axis',(-8.497279155086E-16,-0.923879532511287,-0.382683432365089));
#3274=DIRECTION('ref_axis',(2.05142465794788E-15,0.382683432365089,-0.923879532511287));
#3275=DIRECTION('center_axis',(0.,0.,-1.));
#3276=DIRECTION('ref_axis',(-0.707106781186548,-0.707106781186548,0.));
#3277=DIRECTION('',(0.,0.,-1.));
#3278=DIRECTION('center_axis',(2.05142465794792E-15,-0.382683432365088,
0.923879532511288));
#3279=DIRECTION('ref_axis',(-4.95257723140449E-15,0.923879532511288,0.382683432365088));
#3280=DIRECTION('',(0.,0.,1.));
#3281=DIRECTION('center_axis',(0.,-0.707106781186548,0.707106781186547));
#3282=DIRECTION('ref_axis',(-0.707106781186553,-0.499999999999996,-0.499999999999996));
#3283=DIRECTION('',(0.,0.707106781186548,-0.707106781186547));
#3284=DIRECTION('center_axis',(0.,-0.923879532511286,0.382683432365091));
#3285=DIRECTION('ref_axis',(0.,-0.382683432365091,-0.923879532511286));
#3286=DIRECTION('',(0.,-0.707106781186548,0.707106781186547));
#3287=DIRECTION('center_axis',(0.,-0.707106781186548,-0.707106781186548));
#3288=DIRECTION('ref_axis',(-0.707106781186553,0.499999999999996,-0.499999999999996));
#3289=DIRECTION('',(0.,0.707106781186548,0.707106781186548));
#3290=DIRECTION('center_axis',(0.,-0.382683432365093,-0.923879532511285));
#3291=DIRECTION('ref_axis',(0.,0.923879532511285,-0.382683432365093));
#3292=DIRECTION('',(0.,-0.707106781186548,-0.707106781186548));
#3293=DIRECTION('center_axis',(0.,0.923879532511287,0.38268343236509));
#3294=DIRECTION('ref_axis',(0.,-0.38268343236509,0.923879532511287));
#3295=DIRECTION('center_axis',(0.,0.,1.));
#3296=DIRECTION('ref_axis',(-0.707106781186548,0.707106781186548,0.));
#3297=DIRECTION('',(0.,0.,-1.));
#3298=DIRECTION('',(0.,0.,1.));
#3299=DIRECTION('center_axis',(-4.10284931589583E-15,0.382683432365095,
-0.923879532511285));
#3300=DIRECTION('ref_axis',(9.90515446280873E-15,-0.923879532511285,-0.382683432365095));
#3301=DIRECTION('center_axis',(0.,1.,-2.46716227694479E-17));
#3302=DIRECTION('ref_axis',(-0.70710678118654,0.,-0.707106781186555));
#3303=DIRECTION('',(0.,1.,-2.46716227694479E-17));
#3304=DIRECTION('',(0.,-1.,2.46716227694479E-17));
#3305=DIRECTION('center_axis',(0.,0.707106781186548,-0.707106781186548));
#3306=DIRECTION('ref_axis',(-0.707106781186553,0.499999999999996,0.499999999999996));
#3307=DIRECTION('',(0.,0.707106781186548,-0.707106781186548));
#3308=DIRECTION('',(0.,-0.707106781186548,0.707106781186548));
#3309=DIRECTION('center_axis',(-8.497279155086E-16,0.923879532511287,-0.382683432365089));
#3310=DIRECTION('ref_axis',(-2.05142465794788E-15,0.382683432365089,0.923879532511287));
#3311=DIRECTION('center_axis',(0.,-1.,0.));
#3312=DIRECTION('ref_axis',(-0.70710678118654,0.,0.707106781186555));
#3313=DIRECTION('',(0.,1.,0.));
#3314=DIRECTION('',(0.,-1.,0.));
#3315=DIRECTION('center_axis',(0.,1.,0.));
#3316=DIRECTION('ref_axis',(0.,0.,-1.));
#3317=DIRECTION('',(1.,0.,0.));
#3318=DIRECTION('',(0.,0.,-1.));
#3319=DIRECTION('',(-1.,0.,0.));
#3320=DIRECTION('center_axis',(0.,0.707106781186547,0.707106781186548));
#3321=DIRECTION('ref_axis',(1.,0.,0.));
#3322=DIRECTION('',(-1.,0.,0.));
#3323=DIRECTION('',(0.,0.707106781186548,-0.707106781186547));
#3324=DIRECTION('center_axis',(0.,2.46716227694479E-17,1.));
#3325=DIRECTION('ref_axis',(0.,1.,-2.46716227694479E-17));
#3326=DIRECTION('',(1.,0.,0.));
#3327=DIRECTION('',(0.,1.,-2.46716227694479E-17));
#3328=DIRECTION('center_axis',(0.,-0.707106781186548,0.707106781186548));
#3329=DIRECTION('ref_axis',(1.,0.,0.));
#3330=DIRECTION('',(-1.,0.,0.));
#3331=DIRECTION('',(0.,0.707106781186548,0.707106781186548));
#3332=DIRECTION('center_axis',(1.,0.,0.));
#3333=DIRECTION('ref_axis',(0.,0.,-1.));
#3334=DIRECTION('center_axis',(0.,-0.707106781186548,-0.707106781186548));
#3335=DIRECTION('ref_axis',(-1.,0.,0.));
#3336=DIRECTION('',(-1.,0.,0.));
#3337=DIRECTION('',(0.,-0.707106781186548,0.707106781186548));
#3338=DIRECTION('',(1.,0.,0.));
#3339=DIRECTION('center_axis',(0.,-1.,0.));
#3340=DIRECTION('ref_axis',(0.,0.,1.));
#3341=DIRECTION('',(0.,0.,1.));
#3342=DIRECTION('center_axis',(0.,0.707106781186548,-0.707106781186548));
#3343=DIRECTION('ref_axis',(-1.,0.,0.));
#3344=DIRECTION('',(0.,-0.707106781186548,-0.707106781186548));
#3345=DIRECTION('',(1.,0.,0.));
#3346=DIRECTION('center_axis',(0.,0.,-1.));
#3347=DIRECTION('ref_axis',(0.,-1.,0.));
#3348=DIRECTION('',(0.,-1.,0.));
#3349=DIRECTION('center_axis',(1.,0.,0.));
#3350=DIRECTION('ref_axis',(0.,1.,0.));
#4032=CARTESIAN_POINT('',(0.,0.,0.));
#4033=CARTESIAN_POINT('Origin',(91.,-69.292893218824,34.2928932188156));
#4034=CARTESIAN_POINT('',(90.,-84.5857864376374,19.0000000000021));
#4035=CARTESIAN_POINT('',(90.,-89.0000000000105,14.585786437629));
#4036=CARTESIAN_POINT('',(90.,-69.292893218824,34.2928932188156));
#4037=CARTESIAN_POINT('',(91.,-90.0000000000105,15.0000000000021));
#4038=CARTESIAN_POINT('Origin',(91.,-89.0000000000105,14.585786437629));
#4039=CARTESIAN_POINT('',(91.,-85.0000000000105,20.0000000000021));
#4040=CARTESIAN_POINT('',(91.,-70.0000000000105,35.0000000000021));
#4041=CARTESIAN_POINT('Origin',(91.,-84.5857864376374,19.0000000000021));
#4042=CARTESIAN_POINT('Origin',(91.,-89.0000000000105,10.0000000000021));
#4043=CARTESIAN_POINT('',(90.,-89.0000000000105,-14.5857864376248));
#4044=CARTESIAN_POINT('',(90.,-89.0000000000105,10.0000000000021));
#4045=CARTESIAN_POINT('',(91.,-90.0000000000105,-14.9999999999979));
#4046=CARTESIAN_POINT('Origin',(91.,-89.0000000000105,-14.5857864376248));
#4047=CARTESIAN_POINT('',(91.,-90.0000000000105,10.0000000000021));
#4048=CARTESIAN_POINT('Origin',(91.,-69.292893218824,-34.2928932188113));
#4049=CARTESIAN_POINT('',(90.,-84.5857864376374,-18.9999999999979));
#4050=CARTESIAN_POINT('',(90.,-69.292893218824,-34.2928932188113));
#4051=CARTESIAN_POINT('',(91.,-85.0000000000105,-19.9999999999979));
#4052=CARTESIAN_POINT('Origin',(91.,-84.5857864376374,-18.9999999999979));
#4053=CARTESIAN_POINT('',(91.,-70.0000000000105,-34.9999999999979));
#4054=CARTESIAN_POINT('Origin',(91.,69.2928932188029,-34.2928932188113));
#4055=CARTESIAN_POINT('',(90.,84.5857864376164,-18.9999999999979));
#4056=CARTESIAN_POINT('',(90.,88.9999999999895,-14.5857864376248));
#4057=CARTESIAN_POINT('',(90.,69.2928932188029,-34.2928932188113));
#4058=CARTESIAN_POINT('',(91.,89.9999999999895,-14.9999999999979));
#4059=CARTESIAN_POINT('Origin',(91.,88.9999999999895,-14.5857864376248));
#4060=CARTESIAN_POINT('',(91.,84.9999999999895,-19.9999999999979));
#4061=CARTESIAN_POINT('',(91.,69.9999999999895,-34.9999999999979));
#4062=CARTESIAN_POINT('Origin',(91.,84.5857864376164,-18.9999999999979));
#4063=CARTESIAN_POINT('Origin',(91.,88.9999999999895,-9.99999999999789));
#4064=CARTESIAN_POINT('',(91.,89.9999999999895,15.0000000000021));
#4065=CARTESIAN_POINT('',(91.,89.9999999999895,-9.99999999999789));
#4066=CARTESIAN_POINT('',(90.,88.9999999999895,14.585786437629));
#4067=CARTESIAN_POINT('',(90.,88.9999999999895,-9.99999999999789));
#4068=CARTESIAN_POINT('Origin',(91.,88.9999999999895,14.585786437629));
#4069=CARTESIAN_POINT('Origin',(91.,-45.0000000000105,-18.9999999999979));
#4070=CARTESIAN_POINT('',(90.,-45.0000000000105,-18.9999999999979));
#4071=CARTESIAN_POINT('',(91.,-45.0000000000105,-19.9999999999979));
#4072=CARTESIAN_POINT('Origin',(91.,69.2928932188029,34.2928932188156));
#4073=CARTESIAN_POINT('',(91.,84.9999999999895,20.0000000000021));
#4074=CARTESIAN_POINT('',(91.,69.9999999999895,35.0000000000021));
#4075=CARTESIAN_POINT('',(90.,84.5857864376164,19.0000000000021));
#4076=CARTESIAN_POINT('',(90.,69.2928932188029,34.2928932188156));
#4077=CARTESIAN_POINT('Origin',(91.,84.5857864376164,19.0000000000021));
#4078=CARTESIAN_POINT('Origin',(91.,44.9999999999895,19.0000000000021));
#4079=CARTESIAN_POINT('',(91.,44.9999999999895,20.0000000000021));
#4080=CARTESIAN_POINT('',(90.,44.9999999999895,19.0000000000021));
#4081=CARTESIAN_POINT('Origin',(110.,-90.0000000000105,20.0000000000021));
#4082=CARTESIAN_POINT('',(110.,-90.0000000000105,-14.9999999999979));
#4083=CARTESIAN_POINT('',(110.,-90.0000000000105,-14.9999999999979));
#4084=CARTESIAN_POINT('',(110.,-90.0000000000105,15.0000000000021));
#4085=CARTESIAN_POINT('',(110.,-90.0000000000105,20.0000000000021));
#4086=CARTESIAN_POINT('',(110.,-90.0000000000105,15.0000000000021));
#4087=CARTESIAN_POINT('Origin',(110.,-87.5000000000105,-17.4999999999979));
#4088=CARTESIAN_POINT('',(110.,-85.0000000000105,-19.9999999999979));
#4089=CARTESIAN_POINT('',(110.,-85.0000000000105,-19.9999999999979));
#4090=CARTESIAN_POINT('',(110.,-70.0000000000105,-34.9999999999979));
#4091=CARTESIAN_POINT('Origin',(110.,-90.0000000000105,-19.9999999999979));
#4092=CARTESIAN_POINT('',(110.,84.9999999999895,-19.9999999999979));
#4093=CARTESIAN_POINT('',(110.,84.9999999999895,-19.9999999999979));
#4094=CARTESIAN_POINT('',(110.,-90.0000000000105,-19.9999999999979));
#4095=CARTESIAN_POINT('Origin',(110.,87.4999999999895,-17.4999999999979));
#4096=CARTESIAN_POINT('',(110.,89.9999999999895,-14.9999999999979));
#4097=CARTESIAN_POINT('',(110.,89.9999999999895,-14.9999999999979));
#4098=CARTESIAN_POINT('',(110.,69.9999999999895,-34.9999999999979));
#4099=CARTESIAN_POINT('Origin',(90.,-1.05160324892495E-11,2.1138646388863E-12));
#4100=CARTESIAN_POINT('Origin',(110.,87.4999999999895,17.5000000000021));
#4101=CARTESIAN_POINT('',(110.,84.9999999999895,20.0000000000021));
#4102=CARTESIAN_POINT('',(110.,84.9999999999895,20.0000000000021));
#4103=CARTESIAN_POINT('',(110.,89.9999999999895,15.0000000000021));
#4104=CARTESIAN_POINT('',(110.,69.9999999999895,35.0000000000021));
#4105=CARTESIAN_POINT('',(110.,89.9999999999895,15.0000000000021));
#4106=CARTESIAN_POINT('Origin',(110.,89.9999999999895,-19.9999999999979));
#4107=CARTESIAN_POINT('',(110.,89.9999999999895,-19.9999999999979));
#4108=CARTESIAN_POINT('Origin',(110.,-87.5000000000105,17.5000000000021));
#4109=CARTESIAN_POINT('',(110.,-85.0000000000105,20.0000000000021));
#4110=CARTESIAN_POINT('',(110.,-70.0000000000105,35.0000000000021));
#4111=CARTESIAN_POINT('',(110.,-85.0000000000105,20.0000000000021));
#4112=CARTESIAN_POINT('Origin',(110.,89.9999999999895,20.0000000000021));
#4113=CARTESIAN_POINT('',(110.,89.9999999999895,20.0000000000021));
#4114=CARTESIAN_POINT('Origin',(110.,-1.05160324892495E-11,2.11275441586167E-12));
#4812=UNCERTAINTY_MEASURE_WITH_UNIT(LENGTH_MEASURE(0.01),#4834,
'DISTANCE_ACCURACY_VALUE',
'Maximum model space distance between geometric entities at asserted c
onnectivities');
#4820=UNCERTAINTY_MEASURE_WITH_UNIT(LENGTH_MEASURE(0.01),#4834,
'DISTANCE_ACCURACY_VALUE',
'Maximum model space distance between geometric entities at asserted c
onnectivities');
#4825=(
GEOMETRIC_REPRESENTATION_CONTEXT(3)
GLOBAL_UNCERTAINTY_ASSIGNED_CONTEXT((#4812))
GLOBAL_UNIT_ASSIGNED_CONTEXT((#4834,#4836,#4837))
REPRESENTATION_CONTEXT('','3D')
);
#4833=(
GEOMETRIC_REPRESENTATION_CONTEXT(3)
GLOBAL_UNCERTAINTY_ASSIGNED_CONTEXT((#4820))
GLOBAL_UNIT_ASSIGNED_CONTEXT((#4834,#4836,#4837))
REPRESENTATION_CONTEXT('','3D')
);
#4834=(
LENGTH_UNIT()
NAMED_UNIT(*)
SI_UNIT(.MILLI.,.METRE.)
);
#4836=(
NAMED_UNIT(*)
PLANE_ANGLE_UNIT()
SI_UNIT($,.RADIAN.)
);
#4837=(
NAMED_UNIT(*)
SI_UNIT($,.STERADIAN.)
SOLID_ANGLE_UNIT()
);
#4842=SHAPE_DEFINITION_REPRESENTATION(#4854,#4877);
#4854=PRODUCT_DEFINITION_SHAPE('',$,#4890);
#4877=SHAPE_REPRESENTATION('',(#2889),#4825);
#4885=PRODUCT_DEFINITION_CONTEXT('part definition',#4923,'design');
#4890=PRODUCT_DEFINITION('Front_Block','Front_Block',#4902,#4885);
#4902=PRODUCT_DEFINITION_FORMATION('',$,#4929);
#4923=APPLICATION_CONTEXT(
'Core Data for Automotive Mechanical Design Process');
#4924=PRODUCT_CONTEXT('part definition',#4923,'mechanical');
#4929=PRODUCT('Front_Block','Front_Block',$,(#4924));
#4965=COLOUR_RGB('Dark Blue',0.08,0.2,0.34);
#4966=FILL_AREA_STYLE_COLOUR('',#4965);
#4967=FILL_AREA_STYLE('',(#4966));
#4968=SURFACE_STYLE_FILL_AREA(#4967);
#4969=SURFACE_SIDE_STYLE('',(#4968));
#4970=SURFACE_STYLE_USAGE(.BOTH.,#4969);
#4971=PRESENTATION_STYLE_ASSIGNMENT((#4970));
ENDSEC;
END-ISO-10303-21;
